ISO-10303-21;
HEADER;
/* Generated by software containing ST-Developer
 * from STEP Tools, Inc. (www.steptools.com) 
 */

FILE_DESCRIPTION(
/* description */ ('Belt-driven linear axis on 2020 extrusion'),
/* implementation_level */ '2;1');

FILE_NAME(
/* name */ 'Input M3 set screw (1).step',
/* time_stamp */ '2026-10-28T03:26:09-07:00',
/* author */ (''),
/* organization */ (''),
/* preprocessor_version */ 'ST-DEVELOPER v20.2',
/* originating_system */ 'Autodesk Translation Framework v15.17.0.0',
/* authorisation */ '');

FILE_SCHEMA (('AUTOMOTIVE_DESIGN { 1 0 10303 214 3 1 1 }'));
ENDSEC;

DATA;
#10=MECHANICAL_DESIGN_GEOMETRIC_PRESENTATION_REPRESENTATION('',(#647),#20096);
#545=SHAPE_REPRESENTATION_RELATIONSHIP('SRR','None',#20343,#591);
#591=ADVANCED_BREP_SHAPE_REPRESENTATION('',(#702),#20074);
#647=STYLED_ITEM('',(#20657),#702);
#702=MANIFOLD_SOLID_BREP('Body1',#10961);
#1123=PLANE('',#12243);
#1124=PLANE('',#12244);
#1642=FACE_OUTER_BOUND('',#2384,.T.);
#1643=FACE_OUTER_BOUND('',#2385,.T.);
#1644=FACE_OUTER_BOUND('',#2386,.T.);
#2384=EDGE_LOOP('',(#9031,#9032,#9033,#9034));
#2385=EDGE_LOOP('',(#9035));
#2386=EDGE_LOOP('',(#9036));
#3215=LINE('',#18493,#4072);
#4072=VECTOR('',#14839,0.15);
#4698=CIRCLE('',#12241,0.15);
#4699=CIRCLE('',#12242,0.15);
#5493=VERTEX_POINT('',#18490);
#5494=VERTEX_POINT('',#18492);
#6730=EDGE_CURVE('',#5493,#5493,#4698,.T.);
#6731=EDGE_CURVE('',#5493,#5494,#3215,.T.);
#6732=EDGE_CURVE('',#5494,#5494,#4699,.T.);
#9031=ORIENTED_EDGE('',*,*,#6730,.F.);
#9032=ORIENTED_EDGE('',*,*,#6731,.T.);
#9033=ORIENTED_EDGE('',*,*,#6732,.T.);
#9034=ORIENTED_EDGE('',*,*,#6731,.F.);
#9035=ORIENTED_EDGE('',*,*,#6730,.T.);
#9036=ORIENTED_EDGE('',*,*,#6732,.F.);
#10210=CYLINDRICAL_SURFACE('',#12240,0.15);
#10693=ADVANCED_FACE('',(#1642),#10210,.T.);
#10694=ADVANCED_FACE('',(#1643),#1123,.T.);
#10695=ADVANCED_FACE('',(#1644),#1124,.F.);
#10961=CLOSED_SHELL('',(#10693,#10694,#10695));
#12239=AXIS2_PLACEMENT_3D('',#18488,#14833,#14834);
#12240=AXIS2_PLACEMENT_3D('',#18489,#14835,#14836);
#12241=AXIS2_PLACEMENT_3D('',#18491,#14837,#14838);
#12242=AXIS2_PLACEMENT_3D('',#18494,#14840,#14841);
#12243=AXIS2_PLACEMENT_3D('',#18495,#14842,#14843);
#12244=AXIS2_PLACEMENT_3D('',#18496,#14844,#14845);
#14833=DIRECTION('axis',(0.,0.,1.));
#14834=DIRECTION('refdir',(1.,0.,0.));
#14835=DIRECTION('center_axis',(0.,0.,1.));
#14836=DIRECTION('ref_axis',(1.,0.,0.));
#14837=DIRECTION('center_axis',(0.,0.,1.));
#14838=DIRECTION('ref_axis',(1.,0.,0.));
#14839=DIRECTION('',(0.,0.,-1.));
#14840=DIRECTION('center_axis',(0.,0.,1.));
#14841=DIRECTION('ref_axis',(1.,0.,0.));
#14842=DIRECTION('center_axis',(0.,0.,1.));
#14843=DIRECTION('ref_axis',(1.,0.,0.));
#14844=DIRECTION('center_axis',(0.,0.,1.));
#14845=DIRECTION('ref_axis',(1.,0.,0.));
#18488=CARTESIAN_POINT('',(0.,0.,0.));
#18489=CARTESIAN_POINT('Origin',(0.,-3.95,7.4));
#18490=CARTESIAN_POINT('',(-0.15,-3.95,7.65));
#18491=CARTESIAN_POINT('Origin',(0.,-3.95,7.65));
#18492=CARTESIAN_POINT('',(-0.15,-3.95,7.4));
#18493=CARTESIAN_POINT('',(-0.15,-3.95,7.4));
#18494=CARTESIAN_POINT('Origin',(0.,-3.95,7.4));
#18495=CARTESIAN_POINT('Origin',(0.,-3.95,7.65));
#18496=CARTESIAN_POINT('Origin',(0.,-3.95,7.4));
#20020=UNCERTAINTY_MEASURE_WITH_UNIT(LENGTH_MEASURE(0.001),#20097,
'DISTANCE_ACCURACY_VALUE',
'Maximum model space distance between geometric entities at asserted c
onnectivities');
#20042=UNCERTAINTY_MEASURE_WITH_UNIT(LENGTH_MEASURE(0.001),#20097,
'DISTANCE_ACCURACY_VALUE',
'Maximum model space distance between geometric entities at asserted c
onnectivities');
#20074=(
GEOMETRIC_REPRESENTATION_CONTEXT(3)
GLOBAL_UNCERTAINTY_ASSIGNED_CONTEXT((#20020))
GLOBAL_UNIT_ASSIGNED_CONTEXT((#20097,#20099,#20100))
REPRESENTATION_CONTEXT('','3D')
);
#20096=(
GEOMETRIC_REPRESENTATION_CONTEXT(3)
GLOBAL_UNCERTAINTY_ASSIGNED_CONTEXT((#20042))
GLOBAL_UNIT_ASSIGNED_CONTEXT((#20097,#20099,#20100))
REPRESENTATION_CONTEXT('','3D')
);
#20097=(
LENGTH_UNIT()
NAMED_UNIT(*)
SI_UNIT(.CENTI.,.METRE.)
);
#20099=(
NAMED_UNIT(*)
PLANE_ANGLE_UNIT()
SI_UNIT($,.RADIAN.)
);
#20100=(
NAMED_UNIT(*)
SI_UNIT($,.STERADIAN.)
SOLID_ANGLE_UNIT()
);
#20132=SHAPE_DEFINITION_REPRESENTATION(#20190,#20343);
#20190=PRODUCT_DEFINITION_SHAPE('',$,#20397);
#20343=SHAPE_REPRESENTATION('',(#12239),#20074);
#20365=PRODUCT_DEFINITION_CONTEXT('part definition',#20526,'design');
#20397=PRODUCT_DEFINITION('Input M3 set screw (1)',
'Input M3 set screw (1)',#20450,#20365);
#20450=PRODUCT_DEFINITION_FORMATION('',$,#20559);
#20526=APPLICATION_CONTEXT(
'Core Data for Automotive Mechanical Design Process');
#20527=PRODUCT_CONTEXT('part definition',#20526,'mechanical');
#20559=PRODUCT('Input M3 set screw (1)','Input M3 set screw (1)',
'Input M3 set screw (1)',(#20527));
#20651=COLOUR_RGB('Black',0.12,0.14,0.17);
#20652=FILL_AREA_STYLE_COLOUR('',#20651);
#20653=FILL_AREA_STYLE('',(#20652));
#20654=SURFACE_STYLE_FILL_AREA(#20653);
#20655=SURFACE_SIDE_STYLE('',(#20654));
#20656=SURFACE_STYLE_USAGE(.BOTH.,#20655);
#20657=PRESENTATION_STYLE_ASSIGNMENT((#20656));
ENDSEC;
END-ISO-10303-21;
